ISO-10303-21;
HEADER;
/* Generated by software containing ST-Developer
 * from STEP Tools, Inc. (www.steptools.com) 
 */

FILE_DESCRIPTION(
/* description */ ('Gravity roller conveyor section'),
/* implementation_level */ '2;1');

FILE_NAME(
/* name */ 'Bonded foot pad (1).step',
/* time_stamp */ '2026-11-02T07:43:02-08:00',
/* author */ (''),
/* organization */ (''),
/* preprocessor_version */ 'ST-DEVELOPER v20.2',
/* originating_system */ 'Autodesk Translation Framework v15.17.0.0',
/* authorisation */ '');

FILE_SCHEMA (('AUTOMOTIVE_DESIGN { 1 0 10303 214 3 1 1 }'));
ENDSEC;

DATA;
#10=MECHANICAL_DESIGN_GEOMETRIC_PRESENTATION_REPRESENTATION('',(#539),#13821);
#471=SHAPE_REPRESENTATION_RELATIONSHIP('SRR','None',#14008,#505);
#505=ADVANCED_BREP_SHAPE_REPRESENTATION('',(#579),#13795);
#539=STYLED_ITEM('',(#14193),#579);
#579=MANIFOLD_SOLID_BREP('Body1',#7639);
#889=PLANE('',#8332);
#890=PLANE('',#8333);
#891=PLANE('',#8334);
#892=PLANE('',#8335);
#893=PLANE('',#8336);
#894=PLANE('',#8337);
#1226=FACE_OUTER_BOUND('',#1682,.T.);
#1227=FACE_OUTER_BOUND('',#1683,.T.);
#1228=FACE_OUTER_BOUND('',#1684,.T.);
#1229=FACE_OUTER_BOUND('',#1685,.T.);
#1230=FACE_OUTER_BOUND('',#1686,.T.);
#1231=FACE_OUTER_BOUND('',#1687,.T.);
#1682=EDGE_LOOP('',(#6354,#6355,#6356,#6357));
#1683=EDGE_LOOP('',(#6358,#6359,#6360,#6361));
#1684=EDGE_LOOP('',(#6362,#6363,#6364,#6365));
#1685=EDGE_LOOP('',(#6366,#6367,#6368,#6369));
#1686=EDGE_LOOP('',(#6370,#6371,#6372,#6373));
#1687=EDGE_LOOP('',(#6374,#6375,#6376,#6377));
#2452=LINE('',#12436,#3170);
#2453=LINE('',#12438,#3171);
#2454=LINE('',#12440,#3172);
#2455=LINE('',#12441,#3173);
#2456=LINE('',#12444,#3174);
#2457=LINE('',#12446,#3175);
#2458=LINE('',#12447,#3176);
#2459=LINE('',#12450,#3177);
#2460=LINE('',#12452,#3178);
#2461=LINE('',#12453,#3179);
#2462=LINE('',#12455,#3180);
#2463=LINE('',#12456,#3181);
#3170=VECTOR('',#9901,1.);
#3171=VECTOR('',#9902,1.);
#3172=VECTOR('',#9903,1.);
#3173=VECTOR('',#9904,1.);
#3174=VECTOR('',#9907,1.);
#3175=VECTOR('',#9908,1.);
#3176=VECTOR('',#9909,1.);
#3177=VECTOR('',#9912,1.);
#3178=VECTOR('',#9913,1.);
#3179=VECTOR('',#9914,1.);
#3180=VECTOR('',#9917,1.);
#3181=VECTOR('',#9918,1.);
#3972=VERTEX_POINT('',#12434);
#3973=VERTEX_POINT('',#12435);
#3974=VERTEX_POINT('',#12437);
#3975=VERTEX_POINT('',#12439);
#3976=VERTEX_POINT('',#12443);
#3977=VERTEX_POINT('',#12445);
#3978=VERTEX_POINT('',#12449);
#3979=VERTEX_POINT('',#12451);
#4814=EDGE_CURVE('',#3972,#3973,#2452,.T.);
#4815=EDGE_CURVE('',#3973,#3974,#2453,.T.);
#4816=EDGE_CURVE('',#3975,#3974,#2454,.T.);
#4817=EDGE_CURVE('',#3972,#3975,#2455,.T.);
#4818=EDGE_CURVE('',#3976,#3972,#2456,.T.);
#4819=EDGE_CURVE('',#3977,#3975,#2457,.T.);
#4820=EDGE_CURVE('',#3976,#3977,#2458,.T.);
#4821=EDGE_CURVE('',#3978,#3976,#2459,.T.);
#4822=EDGE_CURVE('',#3979,#3977,#2460,.T.);
#4823=EDGE_CURVE('',#3978,#3979,#2461,.T.);
#4824=EDGE_CURVE('',#3973,#3978,#2462,.T.);
#4825=EDGE_CURVE('',#3974,#3979,#2463,.T.);
#6354=ORIENTED_EDGE('',*,*,#4814,.T.);
#6355=ORIENTED_EDGE('',*,*,#4815,.T.);
#6356=ORIENTED_EDGE('',*,*,#4816,.F.);
#6357=ORIENTED_EDGE('',*,*,#4817,.F.);
#6358=ORIENTED_EDGE('',*,*,#4818,.T.);
#6359=ORIENTED_EDGE('',*,*,#4817,.T.);
#6360=ORIENTED_EDGE('',*,*,#4819,.F.);
#6361=ORIENTED_EDGE('',*,*,#4820,.F.);
#6362=ORIENTED_EDGE('',*,*,#4821,.T.);
#6363=ORIENTED_EDGE('',*,*,#4820,.T.);
#6364=ORIENTED_EDGE('',*,*,#4822,.F.);
#6365=ORIENTED_EDGE('',*,*,#4823,.F.);
#6366=ORIENTED_EDGE('',*,*,#4824,.T.);
#6367=ORIENTED_EDGE('',*,*,#4823,.T.);
#6368=ORIENTED_EDGE('',*,*,#4825,.F.);
#6369=ORIENTED_EDGE('',*,*,#4815,.F.);
#6370=ORIENTED_EDGE('',*,*,#4825,.T.);
#6371=ORIENTED_EDGE('',*,*,#4822,.T.);
#6372=ORIENTED_EDGE('',*,*,#4819,.T.);
#6373=ORIENTED_EDGE('',*,*,#4816,.T.);
#6374=ORIENTED_EDGE('',*,*,#4824,.F.);
#6375=ORIENTED_EDGE('',*,*,#4814,.F.);
#6376=ORIENTED_EDGE('',*,*,#4818,.F.);
#6377=ORIENTED_EDGE('',*,*,#4821,.F.);
#7427=ADVANCED_FACE('',(#1226),#889,.T.);
#7428=ADVANCED_FACE('',(#1227),#890,.T.);
#7429=ADVANCED_FACE('',(#1228),#891,.T.);
#7430=ADVANCED_FACE('',(#1229),#892,.T.);
#7431=ADVANCED_FACE('',(#1230),#893,.T.);
#7432=ADVANCED_FACE('',(#1231),#894,.F.);
#7639=CLOSED_SHELL('',(#7427,#7428,#7429,#7430,#7431,#7432));
#8331=AXIS2_PLACEMENT_3D('',#12432,#9897,#9898);
#8332=AXIS2_PLACEMENT_3D('',#12433,#9899,#9900);
#8333=AXIS2_PLACEMENT_3D('',#12442,#9905,#9906);
#8334=AXIS2_PLACEMENT_3D('',#12448,#9910,#9911);
#8335=AXIS2_PLACEMENT_3D('',#12454,#9915,#9916);
#8336=AXIS2_PLACEMENT_3D('',#12457,#9919,#9920);
#8337=AXIS2_PLACEMENT_3D('',#12458,#9921,#9922);
#9897=DIRECTION('axis',(0.,0.,1.));
#9898=DIRECTION('refdir',(1.,0.,0.));
#9899=DIRECTION('center_axis',(0.,1.,0.));
#9900=DIRECTION('ref_axis',(-1.,0.,0.));
#9901=DIRECTION('',(-1.,0.,0.));
#9902=DIRECTION('',(0.,0.,1.));
#9903=DIRECTION('',(-1.,0.,0.));
#9904=DIRECTION('',(0.,0.,1.));
#9905=DIRECTION('center_axis',(1.,0.,0.));
#9906=DIRECTION('ref_axis',(0.,1.,0.));
#9907=DIRECTION('',(0.,1.,0.));
#9908=DIRECTION('',(0.,1.,0.));
#9909=DIRECTION('',(0.,0.,1.));
#9910=DIRECTION('center_axis',(0.,-1.,0.));
#9911=DIRECTION('ref_axis',(1.,0.,0.));
#9912=DIRECTION('',(1.,0.,0.));
#9913=DIRECTION('',(1.,0.,0.));
#9914=DIRECTION('',(0.,0.,1.));
#9915=DIRECTION('center_axis',(-1.,0.,0.));
#9916=DIRECTION('ref_axis',(0.,-1.,0.));
#9917=DIRECTION('',(0.,-1.,0.));
#9918=DIRECTION('',(0.,-1.,0.));
#9919=DIRECTION('center_axis',(0.,0.,1.));
#9920=DIRECTION('ref_axis',(1.,0.,0.));
#9921=DIRECTION('center_axis',(0.,0.,1.));
#9922=DIRECTION('ref_axis',(1.,0.,0.));
#12432=CARTESIAN_POINT('',(0.,0.,0.));
#12433=CARTESIAN_POINT('Origin',(8.,35.,-17.6));
#12434=CARTESIAN_POINT('',(8.,35.,-17.6));
#12435=CARTESIAN_POINT('',(4.,35.,-17.6));
#12436=CARTESIAN_POINT('',(8.,35.,-17.6));
#12437=CARTESIAN_POINT('',(4.,35.,-16.8));
#12438=CARTESIAN_POINT('',(4.,35.,-17.6));
#12439=CARTESIAN_POINT('',(8.,35.,-16.8));
#12440=CARTESIAN_POINT('',(8.,35.,-16.8));
#12441=CARTESIAN_POINT('',(8.,35.,-17.6));
#12442=CARTESIAN_POINT('Origin',(8.,33.5,-17.6));
#12443=CARTESIAN_POINT('',(8.,33.5,-17.6));
#12444=CARTESIAN_POINT('',(8.,33.5,-17.6));
#12445=CARTESIAN_POINT('',(8.,33.5,-16.8));
#12446=CARTESIAN_POINT('',(8.,33.5,-16.8));
#12447=CARTESIAN_POINT('',(8.,33.5,-17.6));
#12448=CARTESIAN_POINT('Origin',(4.,33.5,-17.6));
#12449=CARTESIAN_POINT('',(4.,33.5,-17.6));
#12450=CARTESIAN_POINT('',(4.,33.5,-17.6));
#12451=CARTESIAN_POINT('',(4.,33.5,-16.8));
#12452=CARTESIAN_POINT('',(4.,33.5,-16.8));
#12453=CARTESIAN_POINT('',(4.,33.5,-17.6));
#12454=CARTESIAN_POINT('Origin',(4.,35.,-17.6));
#12455=CARTESIAN_POINT('',(4.,35.,-17.6));
#12456=CARTESIAN_POINT('',(4.,35.,-16.8));
#12457=CARTESIAN_POINT('Origin',(6.,34.25,-16.8));
#12458=CARTESIAN_POINT('Origin',(6.,34.25,-17.6));
#13756=UNCERTAINTY_MEASURE_WITH_UNIT(LENGTH_MEASURE(0.001),#13822,
'DISTANCE_ACCURACY_VALUE',
'Maximum model space distance between geometric entities at asserted c
onnectivities');
#13782=UNCERTAINTY_MEASURE_WITH_UNIT(LENGTH_MEASURE(0.001),#13822,
'DISTANCE_ACCURACY_VALUE',
'Maximum model space distance between geometric entities at asserted c
onnectivities');
#13795=(
GEOMETRIC_REPRESENTATION_CONTEXT(3)
GLOBAL_UNCERTAINTY_ASSIGNED_CONTEXT((#13756))
GLOBAL_UNIT_ASSIGNED_CONTEXT((#13822,#13824,#13825))
REPRESENTATION_CONTEXT('','3D')
);
#13821=(
GEOMETRIC_REPRESENTATION_CONTEXT(3)
GLOBAL_UNCERTAINTY_ASSIGNED_CONTEXT((#13782))
GLOBAL_UNIT_ASSIGNED_CONTEXT((#13822,#13824,#13825))
REPRESENTATION_CONTEXT('','3D')
);
#13822=(
LENGTH_UNIT()
NAMED_UNIT(*)
SI_UNIT(.CENTI.,.METRE.)
);
#13824=(
NAMED_UNIT(*)
PLANE_ANGLE_UNIT()
SI_UNIT($,.RADIAN.)
);
#13825=(
NAMED_UNIT(*)
SI_UNIT($,.STERADIAN.)
SOLID_ANGLE_UNIT()
);
#13838=SHAPE_DEFINITION_REPRESENTATION(#13876,#14008);
#13876=PRODUCT_DEFINITION_SHAPE('',$,#14047);
#14008=SHAPE_REPRESENTATION('',(#8331),#13795);
#14034=PRODUCT_DEFINITION_CONTEXT('part definition',#14150,'design');
#14047=PRODUCT_DEFINITION('Bonded foot pad_1','Bonded foot pad (1)',#14085,
#14034);
#14085=PRODUCT_DEFINITION_FORMATION('',$,#14164);
#14150=APPLICATION_CONTEXT(
'Core Data for Automotive Mechanical Design Process');
#14151=PRODUCT_CONTEXT('part definition',#14150,'mechanical');
#14164=PRODUCT('Bonded foot pad_1','Bonded foot pad (1)',
'Bonded foot pad',(#14151));
#14193=PRESENTATION_STYLE_ASSIGNMENT((#14198));
#14198=SURFACE_STYLE_USAGE(.BOTH.,#14203);
#14203=SURFACE_SIDE_STYLE('',(#14208));
#14208=SURFACE_STYLE_FILL_AREA(#14213);
#14213=FILL_AREA_STYLE('CAD Library Painted - Graphite',(#14218));
#14218=FILL_AREA_STYLE_COLOUR('CAD Library Painted - Graphite',#14223);
#14223=COLOUR_RGB('CAD Library Painted - Graphite',0.168627450980392,0.192156862745098,
0.231372549019608);
ENDSEC;
END-ISO-10303-21;
